ISO-10303-21;
HEADER;
/* Generated by software containing ST-Developer
 * from STEP Tools, Inc. (www.steptools.com) 
 */

FILE_DESCRIPTION(
/* description */ (''),
/* implementation_level */ '2;1');

FILE_NAME(
/* name */ 'Bottom_Base.step',
/* time_stamp */ '2026-10-05T15:35:09-07:00',
/* author */ (''),
/* organization */ (''),
/* preprocessor_version */ 'ST-DEVELOPER v20.2',
/* originating_system */ 'Autodesk Translation Framework v15.15.0.0',
/* authorisation */ '');

FILE_SCHEMA (('AUTOMOTIVE_DESIGN { 1 0 10303 214 3 1 1 }'));
ENDSEC;

DATA;
#10=MECHANICAL_DESIGN_GEOMETRIC_PRESENTATION_REPRESENTATION('',(#543),#74523);
#525=SHAPE_REPRESENTATION_RELATIONSHIP('SRR','None',#74558,#534);
#534=ADVANCED_BREP_SHAPE_REPRESENTATION('',(#552),#74514);
#543=STYLED_ITEM('',(#74612),#552);
#552=MANIFOLD_SOLID_BREP('Body1',#4722);
#561=FACE_BOUND('',#834,.T.);
#562=FACE_BOUND('',#835,.T.);
#563=FACE_BOUND('',#839,.T.);
#564=FACE_BOUND('',#840,.T.);
#565=FACE_BOUND('',#848,.T.);
#566=FACE_BOUND('',#849,.T.);
#567=FACE_BOUND('',#855,.T.);
#568=FACE_BOUND('',#856,.T.);
#609=PLANE('',#4845);
#610=PLANE('',#4846);
#611=PLANE('',#4850);
#612=PLANE('',#4857);
#613=PLANE('',#4861);
#614=PLANE('',#4862);
#615=PLANE('',#4867);
#616=PLANE('',#4868);
#617=PLANE('',#4871);
#618=PLANE('',#4874);
#619=PLANE('',#4875);
#620=PLANE('',#4878);
#621=PLANE('',#4881);
#622=PLANE('',#4882);
#682=FACE_OUTER_BOUND('',#826,.T.);
#683=FACE_OUTER_BOUND('',#827,.T.);
#684=FACE_OUTER_BOUND('',#828,.T.);
#685=FACE_OUTER_BOUND('',#829,.T.);
#686=FACE_OUTER_BOUND('',#830,.T.);
#687=FACE_OUTER_BOUND('',#831,.T.);
#688=FACE_OUTER_BOUND('',#832,.T.);
#689=FACE_OUTER_BOUND('',#833,.T.);
#690=FACE_OUTER_BOUND('',#836,.T.);
#691=FACE_OUTER_BOUND('',#837,.T.);
#692=FACE_OUTER_BOUND('',#838,.T.);
#693=FACE_OUTER_BOUND('',#841,.T.);
#694=FACE_OUTER_BOUND('',#842,.T.);
#695=FACE_OUTER_BOUND('',#843,.T.);
#696=FACE_OUTER_BOUND('',#844,.T.);
#697=FACE_OUTER_BOUND('',#845,.T.);
#698=FACE_OUTER_BOUND('',#846,.T.);
#699=FACE_OUTER_BOUND('',#847,.T.);
#700=FACE_OUTER_BOUND('',#850,.T.);
#701=FACE_OUTER_BOUND('',#851,.T.);
#702=FACE_OUTER_BOUND('',#852,.T.);
#703=FACE_OUTER_BOUND('',#853,.T.);
#704=FACE_OUTER_BOUND('',#854,.T.);
#705=FACE_OUTER_BOUND('',#857,.T.);
#706=FACE_OUTER_BOUND('',#858,.T.);
#707=FACE_OUTER_BOUND('',#859,.T.);
#826=EDGE_LOOP('',(#2958,#2959,#2960,#2961));
#827=EDGE_LOOP('',(#2962,#2963,#2964,#2965));
#828=EDGE_LOOP('',(#2966,#2967,#2968,#2969));
#829=EDGE_LOOP('',(#2970,#2971,#2972,#2973));
#830=EDGE_LOOP('',(#2974,#2975,#2976,#2977));
#831=EDGE_LOOP('',(#2978,#2979,#2980,#2981));
#832=EDGE_LOOP('',(#2982,#2983,#2984,#2985));
#833=EDGE_LOOP('',(#2986,#2987,#2988,#2989));
#834=EDGE_LOOP('',(#2990));
#835=EDGE_LOOP('',(#2991));
#836=EDGE_LOOP('',(#2992,#2993,#2994,#2995));
#837=EDGE_LOOP('',(#2996,#2997,#2998,#2999));
#838=EDGE_LOOP('',(#3000,#3001,#3002,#3003));
#839=EDGE_LOOP('',(#3004));
#840=EDGE_LOOP('',(#3005));
#841=EDGE_LOOP('',(#3006,#3007,#3008,#3009));
#842=EDGE_LOOP('',(#3010,#3011,#3012,#3013));
#843=EDGE_LOOP('',(#3014,#3015,#3016,#3017,#3018,#3019,#3020,#3021,#3022,
#3023,#3024,#3025,#3026,#3027,#3028,#3029,#3030,#3031,#3032,#3033));
#844=EDGE_LOOP('',(#3034,#3035,#3036,#3037));
#845=EDGE_LOOP('',(#3038,#3039,#3040,#3041));
#846=EDGE_LOOP('',(#3042,#3043,#3044,#3045));
#847=EDGE_LOOP('',(#3046,#3047,#3048,#3049));
#848=EDGE_LOOP('',(#3050));
#849=EDGE_LOOP('',(#3051));
#850=EDGE_LOOP('',(#3052,#3053,#3054,#3055));
#851=EDGE_LOOP('',(#3056,#3057,#3058,#3059));
#852=EDGE_LOOP('',(#3060,#3061,#3062,#3063));
#853=EDGE_LOOP('',(#3064,#3065,#3066,#3067));
#854=EDGE_LOOP('',(#3068,#3069,#3070,#3071));
#855=EDGE_LOOP('',(#3072));
#856=EDGE_LOOP('',(#3073));
#857=EDGE_LOOP('',(#3074,#3075,#3076,#3077));
#858=EDGE_LOOP('',(#3078,#3079,#3080,#3081));
#859=EDGE_LOOP('',(#3082,#3083,#3084,#3085,#3086,#3087,#3088,#3089,#3090,
#3091,#3092,#3093,#3094,#3095,#3096,#3097,#3098,#3099,#3100,#3101));
#1018=LINE('',#5835,#1215);
#1019=LINE('',#5841,#1216);
#1020=LINE('',#5847,#1217);
#1021=LINE('',#5853,#1218);
#1022=LINE('',#5858,#1219);
#1023=LINE('',#5860,#1220);
#1024=LINE('',#5862,#1221);
#1025=LINE('',#5863,#1222);
#1026=LINE('',#5866,#1223);
#1027=LINE('',#5868,#1224);
#1028=LINE('',#5869,#1225);
#1029=LINE('',#5874,#1226);
#1030=LINE('',#5878,#1227);
#1031=LINE('',#5880,#1228);
#1032=LINE('',#5881,#1229);
#1033=LINE('',#5886,#1230);
#1034=LINE('',#5891,#1231);
#1035=LINE('',#5895,#1232);
#1036=LINE('',#5899,#1233);
#1037=LINE('',#5901,#1234);
#1038=LINE('',#5902,#1235);
#1039=LINE('',#5907,#1236);
#1040=LINE('',#5910,#1237);
#1041=LINE('',#5911,#1238);
#1042=LINE('',#5915,#1239);
#1043=LINE('',#5917,#1240);
#1044=LINE('',#5919,#1241);
#1045=LINE('',#5923,#1242);
#1046=LINE('',#5926,#1243);
#1047=LINE('',#5928,#1244);
#1048=LINE('',#5932,#1245);
#1049=LINE('',#5936,#1246);
#1050=LINE('',#5938,#1247);
#1051=LINE('',#5939,#1248);
#1052=LINE('',#5942,#1249);
#1053=LINE('',#5943,#1250);
#1054=LINE('',#5947,#1251);
#1055=LINE('',#5950,#1252);
#1056=LINE('',#5951,#1253);
#1057=LINE('',#5955,#1254);
#1058=LINE('',#5957,#1255);
#1059=LINE('',#5960,#1256);
#1060=LINE('',#5961,#1257);
#1061=LINE('',#5965,#1258);
#1062=LINE('',#5968,#1259);
#1063=LINE('',#5969,#1260);
#1064=LINE('',#5973,#1261);
#1065=LINE('',#5975,#1262);
#1215=VECTOR('',#5106,7.5);
#1216=VECTOR('',#5113,7.5);
#1217=VECTOR('',#5120,7.5);
#1218=VECTOR('',#5127,7.5);
#1219=VECTOR('',#5132,10.);
#1220=VECTOR('',#5133,10.);
#1221=VECTOR('',#5134,10.);
#1222=VECTOR('',#5135,10.);
#1223=VECTOR('',#5138,10.);
#1224=VECTOR('',#5139,10.);
#1225=VECTOR('',#5140,10.);
#1226=VECTOR('',#5145,10.);
#1227=VECTOR('',#5150,10.);
#1228=VECTOR('',#5151,10.);
#1229=VECTOR('',#5152,10.);
#1230=VECTOR('',#5157,10.);
#1231=VECTOR('',#5162,10.);
#1232=VECTOR('',#5165,10.);
#1233=VECTOR('',#5170,10.);
#1234=VECTOR('',#5171,10.);
#1235=VECTOR('',#5172,10.);
#1236=VECTOR('',#5177,10.);
#1237=VECTOR('',#5182,10.);
#1238=VECTOR('',#5183,10.);
#1239=VECTOR('',#5186,10.);
#1240=VECTOR('',#5187,10.);
#1241=VECTOR('',#5188,10.);
#1242=VECTOR('',#5191,10.);
#1243=VECTOR('',#5194,10.);
#1244=VECTOR('',#5195,10.);
#1245=VECTOR('',#5198,10.);
#1246=VECTOR('',#5203,10.);
#1247=VECTOR('',#5204,10.);
#1248=VECTOR('',#5205,10.);
#1249=VECTOR('',#5208,10.);
#1250=VECTOR('',#5209,10.);
#1251=VECTOR('',#5214,10.);
#1252=VECTOR('',#5217,10.);
#1253=VECTOR('',#5218,10.);
#1254=VECTOR('',#5223,10.);
#1255=VECTOR('',#5226,10.);
#1256=VECTOR('',#5229,10.);
#1257=VECTOR('',#5230,10.);
#1258=VECTOR('',#5235,10.);
#1259=VECTOR('',#5238,10.);
#1260=VECTOR('',#5239,10.);
#1261=VECTOR('',#5244,10.);
#1262=VECTOR('',#5247,10.);
#1412=CIRCLE('',#4834,7.5);
#1413=CIRCLE('',#4835,7.5);
#1414=CIRCLE('',#4837,7.5);
#1415=CIRCLE('',#4838,7.5);
#1416=CIRCLE('',#4840,7.5);
#1417=CIRCLE('',#4841,7.5);
#1418=CIRCLE('',#4843,7.5);
#1419=CIRCLE('',#4844,7.5);
#1420=CIRCLE('',#4848,3.00000000000002);
#1421=CIRCLE('',#4849,3.00000000000002);
#1422=CIRCLE('',#4852,3.00000000000002);
#1423=CIRCLE('',#4853,3.00000000000002);
#1424=CIRCLE('',#4855,3.00000000000002);
#1425=CIRCLE('',#4856,3.00000000000002);
#1426=CIRCLE('',#4859,3.00000000000002);
#1427=CIRCLE('',#4860,3.00000000000002);
#1428=CIRCLE('',#4863,3.00000000000002);
#1429=CIRCLE('',#4864,3.00000000000002);
#1430=CIRCLE('',#4865,3.00000000000002);
#1431=CIRCLE('',#4866,3.00000000000002);
#1432=CIRCLE('',#4870,3.00000000000002);
#1433=CIRCLE('',#4873,3.00000000000002);
#1434=CIRCLE('',#4877,3.00000000000002);
#1435=CIRCLE('',#4880,3.00000000000002);
#1522=VERTEX_POINT('',#5832);
#1523=VERTEX_POINT('',#5834);
#1524=VERTEX_POINT('',#5838);
#1525=VERTEX_POINT('',#5840);
#1526=VERTEX_POINT('',#5844);
#1527=VERTEX_POINT('',#5846);
#1528=VERTEX_POINT('',#5850);
#1529=VERTEX_POINT('',#5852);
#1530=VERTEX_POINT('',#5856);
#1531=VERTEX_POINT('',#5857);
#1532=VERTEX_POINT('',#5859);
#1533=VERTEX_POINT('',#5861);
#1534=VERTEX_POINT('',#5865);
#1535=VERTEX_POINT('',#5867);
#1536=VERTEX_POINT('',#5871);
#1537=VERTEX_POINT('',#5873);
#1538=VERTEX_POINT('',#5877);
#1539=VERTEX_POINT('',#5879);
#1540=VERTEX_POINT('',#5883);
#1541=VERTEX_POINT('',#5885);
#1542=VERTEX_POINT('',#5889);
#1543=VERTEX_POINT('',#5890);
#1544=VERTEX_POINT('',#5892);
#1545=VERTEX_POINT('',#5894);
#1546=VERTEX_POINT('',#5898);
#1547=VERTEX_POINT('',#5900);
#1548=VERTEX_POINT('',#5904);
#1549=VERTEX_POINT('',#5906);
#1550=VERTEX_POINT('',#5913);
#1551=VERTEX_POINT('',#5914);
#1552=VERTEX_POINT('',#5916);
#1553=VERTEX_POINT('',#5918);
#1554=VERTEX_POINT('',#5920);
#1555=VERTEX_POINT('',#5922);
#1556=VERTEX_POINT('',#5924);
#1557=VERTEX_POINT('',#5927);
#1558=VERTEX_POINT('',#5929);
#1559=VERTEX_POINT('',#5931);
#1560=VERTEX_POINT('',#5935);
#1561=VERTEX_POINT('',#5937);
#1562=VERTEX_POINT('',#5941);
#1563=VERTEX_POINT('',#5945);
#1564=VERTEX_POINT('',#5949);
#1565=VERTEX_POINT('',#5953);
#1566=VERTEX_POINT('',#5959);
#1567=VERTEX_POINT('',#5963);
#1568=VERTEX_POINT('',#5967);
#1569=VERTEX_POINT('',#5971);
#2180=EDGE_CURVE('',#1522,#1522,#1412,.T.);
#2181=EDGE_CURVE('',#1522,#1523,#1018,.T.);
#2182=EDGE_CURVE('',#1523,#1523,#1413,.T.);
#2183=EDGE_CURVE('',#1524,#1524,#1414,.T.);
#2184=EDGE_CURVE('',#1524,#1525,#1019,.T.);
#2185=EDGE_CURVE('',#1525,#1525,#1415,.T.);
#2186=EDGE_CURVE('',#1526,#1526,#1416,.T.);
#2187=EDGE_CURVE('',#1526,#1527,#1020,.T.);
#2188=EDGE_CURVE('',#1527,#1527,#1417,.T.);
#2189=EDGE_CURVE('',#1528,#1528,#1418,.T.);
#2190=EDGE_CURVE('',#1528,#1529,#1021,.T.);
#2191=EDGE_CURVE('',#1529,#1529,#1419,.T.);
#2192=EDGE_CURVE('',#1530,#1531,#1022,.T.);
#2193=EDGE_CURVE('',#1531,#1532,#1023,.T.);
#2194=EDGE_CURVE('',#1532,#1533,#1024,.T.);
#2195=EDGE_CURVE('',#1533,#1530,#1025,.T.);
#2196=EDGE_CURVE('',#1532,#1534,#1026,.T.);
#2197=EDGE_CURVE('',#1534,#1535,#1027,.T.);
#2198=EDGE_CURVE('',#1535,#1533,#1028,.T.);
#2199=EDGE_CURVE('',#1534,#1536,#1420,.T.);
#2200=EDGE_CURVE('',#1536,#1537,#1029,.T.);
#2201=EDGE_CURVE('',#1537,#1535,#1421,.T.);
#2202=EDGE_CURVE('',#1536,#1538,#1030,.T.);
#2203=EDGE_CURVE('',#1538,#1539,#1031,.T.);
#2204=EDGE_CURVE('',#1539,#1537,#1032,.T.);
#2205=EDGE_CURVE('',#1538,#1540,#1422,.T.);
#2206=EDGE_CURVE('',#1540,#1541,#1033,.T.);
#2207=EDGE_CURVE('',#1541,#1539,#1423,.T.);
#2208=EDGE_CURVE('',#1542,#1543,#1034,.T.);
#2209=EDGE_CURVE('',#1542,#1544,#1424,.T.);
#2210=EDGE_CURVE('',#1544,#1545,#1035,.T.);
#2211=EDGE_CURVE('',#1545,#1543,#1425,.T.);
#2212=EDGE_CURVE('',#1544,#1546,#1036,.T.);
#2213=EDGE_CURVE('',#1546,#1547,#1037,.T.);
#2214=EDGE_CURVE('',#1547,#1545,#1038,.T.);
#2215=EDGE_CURVE('',#1546,#1548,#1426,.T.);
#2216=EDGE_CURVE('',#1548,#1549,#1039,.T.);
#2217=EDGE_CURVE('',#1549,#1547,#1427,.T.);
#2218=EDGE_CURVE('',#1548,#1531,#1040,.T.);
#2219=EDGE_CURVE('',#1530,#1549,#1041,.T.);
#2220=EDGE_CURVE('',#1550,#1551,#1042,.T.);
#2221=EDGE_CURVE('',#1551,#1552,#1043,.T.);
#2222=EDGE_CURVE('',#1552,#1553,#1044,.T.);
#2223=EDGE_CURVE('',#1553,#1554,#1428,.T.);
#2224=EDGE_CURVE('',#1554,#1555,#1045,.T.);
#2225=EDGE_CURVE('',#1555,#1556,#1429,.T.);
#2226=EDGE_CURVE('',#1556,#1540,#1046,.T.);
#2227=EDGE_CURVE('',#1557,#1542,#1047,.T.);
#2228=EDGE_CURVE('',#1557,#1558,#1430,.T.);
#2229=EDGE_CURVE('',#1558,#1559,#1048,.T.);
#2230=EDGE_CURVE('',#1559,#1550,#1431,.T.);
#2231=EDGE_CURVE('',#1560,#1551,#1049,.T.);
#2232=EDGE_CURVE('',#1561,#1560,#1050,.T.);
#2233=EDGE_CURVE('',#1552,#1561,#1051,.T.);
#2234=EDGE_CURVE('',#1562,#1561,#1052,.T.);
#2235=EDGE_CURVE('',#1553,#1562,#1053,.T.);
#2236=EDGE_CURVE('',#1563,#1562,#1432,.T.);
#2237=EDGE_CURVE('',#1554,#1563,#1054,.T.);
#2238=EDGE_CURVE('',#1564,#1563,#1055,.T.);
#2239=EDGE_CURVE('',#1555,#1564,#1056,.T.);
#2240=EDGE_CURVE('',#1565,#1564,#1433,.T.);
#2241=EDGE_CURVE('',#1556,#1565,#1057,.T.);
#2242=EDGE_CURVE('',#1565,#1541,#1058,.T.);
#2243=EDGE_CURVE('',#1566,#1543,#1059,.T.);
#2244=EDGE_CURVE('',#1557,#1566,#1060,.T.);
#2245=EDGE_CURVE('',#1567,#1566,#1434,.T.);
#2246=EDGE_CURVE('',#1558,#1567,#1061,.T.);
#2247=EDGE_CURVE('',#1568,#1567,#1062,.T.);
#2248=EDGE_CURVE('',#1559,#1568,#1063,.T.);
#2249=EDGE_CURVE('',#1569,#1568,#1435,.T.);
#2250=EDGE_CURVE('',#1550,#1569,#1064,.T.);
#2251=EDGE_CURVE('',#1560,#1569,#1065,.T.);
#2958=ORIENTED_EDGE('',*,*,#2180,.F.);
#2959=ORIENTED_EDGE('',*,*,#2181,.T.);
#2960=ORIENTED_EDGE('',*,*,#2182,.F.);
#2961=ORIENTED_EDGE('',*,*,#2181,.F.);
#2962=ORIENTED_EDGE('',*,*,#2183,.F.);
#2963=ORIENTED_EDGE('',*,*,#2184,.T.);
#2964=ORIENTED_EDGE('',*,*,#2185,.F.);
#2965=ORIENTED_EDGE('',*,*,#2184,.F.);
#2966=ORIENTED_EDGE('',*,*,#2186,.F.);
#2967=ORIENTED_EDGE('',*,*,#2187,.T.);
#2968=ORIENTED_EDGE('',*,*,#2188,.F.);
#2969=ORIENTED_EDGE('',*,*,#2187,.F.);
#2970=ORIENTED_EDGE('',*,*,#2189,.F.);
#2971=ORIENTED_EDGE('',*,*,#2190,.T.);
#2972=ORIENTED_EDGE('',*,*,#2191,.F.);
#2973=ORIENTED_EDGE('',*,*,#2190,.F.);
#2974=ORIENTED_EDGE('',*,*,#2192,.T.);
#2975=ORIENTED_EDGE('',*,*,#2193,.T.);
#2976=ORIENTED_EDGE('',*,*,#2194,.T.);
#2977=ORIENTED_EDGE('',*,*,#2195,.T.);
#2978=ORIENTED_EDGE('',*,*,#2194,.F.);
#2979=ORIENTED_EDGE('',*,*,#2196,.T.);
#2980=ORIENTED_EDGE('',*,*,#2197,.T.);
#2981=ORIENTED_EDGE('',*,*,#2198,.T.);
#2982=ORIENTED_EDGE('',*,*,#2197,.F.);
#2983=ORIENTED_EDGE('',*,*,#2199,.T.);
#2984=ORIENTED_EDGE('',*,*,#2200,.T.);
#2985=ORIENTED_EDGE('',*,*,#2201,.T.);
#2986=ORIENTED_EDGE('',*,*,#2200,.F.);
#2987=ORIENTED_EDGE('',*,*,#2202,.T.);
#2988=ORIENTED_EDGE('',*,*,#2203,.T.);
#2989=ORIENTED_EDGE('',*,*,#2204,.T.);
#2990=ORIENTED_EDGE('',*,*,#2183,.T.);
#2991=ORIENTED_EDGE('',*,*,#2189,.T.);
#2992=ORIENTED_EDGE('',*,*,#2203,.F.);
#2993=ORIENTED_EDGE('',*,*,#2205,.T.);
#2994=ORIENTED_EDGE('',*,*,#2206,.T.);
#2995=ORIENTED_EDGE('',*,*,#2207,.T.);
#2996=ORIENTED_EDGE('',*,*,#2208,.F.);
#2997=ORIENTED_EDGE('',*,*,#2209,.T.);
#2998=ORIENTED_EDGE('',*,*,#2210,.T.);
#2999=ORIENTED_EDGE('',*,*,#2211,.T.);
#3000=ORIENTED_EDGE('',*,*,#2210,.F.);
#3001=ORIENTED_EDGE('',*,*,#2212,.T.);
#3002=ORIENTED_EDGE('',*,*,#2213,.T.);
#3003=ORIENTED_EDGE('',*,*,#2214,.T.);
#3004=ORIENTED_EDGE('',*,*,#2185,.T.);
#3005=ORIENTED_EDGE('',*,*,#2191,.T.);
#3006=ORIENTED_EDGE('',*,*,#2213,.F.);
#3007=ORIENTED_EDGE('',*,*,#2215,.T.);
#3008=ORIENTED_EDGE('',*,*,#2216,.T.);
#3009=ORIENTED_EDGE('',*,*,#2217,.T.);
#3010=ORIENTED_EDGE('',*,*,#2216,.F.);
#3011=ORIENTED_EDGE('',*,*,#2218,.T.);
#3012=ORIENTED_EDGE('',*,*,#2192,.F.);
#3013=ORIENTED_EDGE('',*,*,#2219,.T.);
#3014=ORIENTED_EDGE('',*,*,#2220,.T.);
#3015=ORIENTED_EDGE('',*,*,#2221,.T.);
#3016=ORIENTED_EDGE('',*,*,#2222,.T.);
#3017=ORIENTED_EDGE('',*,*,#2223,.T.);
#3018=ORIENTED_EDGE('',*,*,#2224,.T.);
#3019=ORIENTED_EDGE('',*,*,#2225,.T.);
#3020=ORIENTED_EDGE('',*,*,#2226,.T.);
#3021=ORIENTED_EDGE('',*,*,#2205,.F.);
#3022=ORIENTED_EDGE('',*,*,#2202,.F.);
#3023=ORIENTED_EDGE('',*,*,#2199,.F.);
#3024=ORIENTED_EDGE('',*,*,#2196,.F.);
#3025=ORIENTED_EDGE('',*,*,#2193,.F.);
#3026=ORIENTED_EDGE('',*,*,#2218,.F.);
#3027=ORIENTED_EDGE('',*,*,#2215,.F.);
#3028=ORIENTED_EDGE('',*,*,#2212,.F.);
#3029=ORIENTED_EDGE('',*,*,#2209,.F.);
#3030=ORIENTED_EDGE('',*,*,#2227,.F.);
#3031=ORIENTED_EDGE('',*,*,#2228,.T.);
#3032=ORIENTED_EDGE('',*,*,#2229,.T.);
#3033=ORIENTED_EDGE('',*,*,#2230,.T.);
#3034=ORIENTED_EDGE('',*,*,#2231,.F.);
#3035=ORIENTED_EDGE('',*,*,#2232,.F.);
#3036=ORIENTED_EDGE('',*,*,#2233,.F.);
#3037=ORIENTED_EDGE('',*,*,#2221,.F.);
#3038=ORIENTED_EDGE('',*,*,#2233,.T.);
#3039=ORIENTED_EDGE('',*,*,#2234,.F.);
#3040=ORIENTED_EDGE('',*,*,#2235,.F.);
#3041=ORIENTED_EDGE('',*,*,#2222,.F.);
#3042=ORIENTED_EDGE('',*,*,#2235,.T.);
#3043=ORIENTED_EDGE('',*,*,#2236,.F.);
#3044=ORIENTED_EDGE('',*,*,#2237,.F.);
#3045=ORIENTED_EDGE('',*,*,#2223,.F.);
#3046=ORIENTED_EDGE('',*,*,#2237,.T.);
#3047=ORIENTED_EDGE('',*,*,#2238,.F.);
#3048=ORIENTED_EDGE('',*,*,#2239,.F.);
#3049=ORIENTED_EDGE('',*,*,#2224,.F.);
#3050=ORIENTED_EDGE('',*,*,#2182,.T.);
#3051=ORIENTED_EDGE('',*,*,#2188,.T.);
#3052=ORIENTED_EDGE('',*,*,#2239,.T.);
#3053=ORIENTED_EDGE('',*,*,#2240,.F.);
#3054=ORIENTED_EDGE('',*,*,#2241,.F.);
#3055=ORIENTED_EDGE('',*,*,#2225,.F.);
#3056=ORIENTED_EDGE('',*,*,#2241,.T.);
#3057=ORIENTED_EDGE('',*,*,#2242,.T.);
#3058=ORIENTED_EDGE('',*,*,#2206,.F.);
#3059=ORIENTED_EDGE('',*,*,#2226,.F.);
#3060=ORIENTED_EDGE('',*,*,#2243,.F.);
#3061=ORIENTED_EDGE('',*,*,#2244,.F.);
#3062=ORIENTED_EDGE('',*,*,#2227,.T.);
#3063=ORIENTED_EDGE('',*,*,#2208,.T.);
#3064=ORIENTED_EDGE('',*,*,#2244,.T.);
#3065=ORIENTED_EDGE('',*,*,#2245,.F.);
#3066=ORIENTED_EDGE('',*,*,#2246,.F.);
#3067=ORIENTED_EDGE('',*,*,#2228,.F.);
#3068=ORIENTED_EDGE('',*,*,#2246,.T.);
#3069=ORIENTED_EDGE('',*,*,#2247,.F.);
#3070=ORIENTED_EDGE('',*,*,#2248,.F.);
#3071=ORIENTED_EDGE('',*,*,#2229,.F.);
#3072=ORIENTED_EDGE('',*,*,#2180,.T.);
#3073=ORIENTED_EDGE('',*,*,#2186,.T.);
#3074=ORIENTED_EDGE('',*,*,#2248,.T.);
#3075=ORIENTED_EDGE('',*,*,#2249,.F.);
#3076=ORIENTED_EDGE('',*,*,#2250,.F.);
#3077=ORIENTED_EDGE('',*,*,#2230,.F.);
#3078=ORIENTED_EDGE('',*,*,#2250,.T.);
#3079=ORIENTED_EDGE('',*,*,#2251,.F.);
#3080=ORIENTED_EDGE('',*,*,#2231,.T.);
#3081=ORIENTED_EDGE('',*,*,#2220,.F.);
#3082=ORIENTED_EDGE('',*,*,#2251,.T.);
#3083=ORIENTED_EDGE('',*,*,#2249,.T.);
#3084=ORIENTED_EDGE('',*,*,#2247,.T.);
#3085=ORIENTED_EDGE('',*,*,#2245,.T.);
#3086=ORIENTED_EDGE('',*,*,#2243,.T.);
#3087=ORIENTED_EDGE('',*,*,#2211,.F.);
#3088=ORIENTED_EDGE('',*,*,#2214,.F.);
#3089=ORIENTED_EDGE('',*,*,#2217,.F.);
#3090=ORIENTED_EDGE('',*,*,#2219,.F.);
#3091=ORIENTED_EDGE('',*,*,#2195,.F.);
#3092=ORIENTED_EDGE('',*,*,#2198,.F.);
#3093=ORIENTED_EDGE('',*,*,#2201,.F.);
#3094=ORIENTED_EDGE('',*,*,#2204,.F.);
#3095=ORIENTED_EDGE('',*,*,#2207,.F.);
#3096=ORIENTED_EDGE('',*,*,#2242,.F.);
#3097=ORIENTED_EDGE('',*,*,#2240,.T.);
#3098=ORIENTED_EDGE('',*,*,#2238,.T.);
#3099=ORIENTED_EDGE('',*,*,#2236,.T.);
#3100=ORIENTED_EDGE('',*,*,#2234,.T.);
#3101=ORIENTED_EDGE('',*,*,#2232,.T.);
#4514=CYLINDRICAL_SURFACE('',#4833,7.5);
#4515=CYLINDRICAL_SURFACE('',#4836,7.5);
#4516=CYLINDRICAL_SURFACE('',#4839,7.5);
#4517=CYLINDRICAL_SURFACE('',#4842,7.5);
#4518=CYLINDRICAL_SURFACE('',#4847,3.00000000000002);
#4519=CYLINDRICAL_SURFACE('',#4851,3.00000000000002);
#4520=CYLINDRICAL_SURFACE('',#4854,3.00000000000002);
#4521=CYLINDRICAL_SURFACE('',#4858,3.00000000000002);
#4522=CYLINDRICAL_SURFACE('',#4869,3.00000000000002);
#4523=CYLINDRICAL_SURFACE('',#4872,3.00000000000002);
#4524=CYLINDRICAL_SURFACE('',#4876,3.00000000000002);
#4525=CYLINDRICAL_SURFACE('',#4879,3.00000000000002);
#4578=ADVANCED_FACE('',(#682),#4514,.F.);
#4579=ADVANCED_FACE('',(#683),#4515,.F.);
#4580=ADVANCED_FACE('',(#684),#4516,.F.);
#4581=ADVANCED_FACE('',(#685),#4517,.F.);
#4582=ADVANCED_FACE('',(#686),#609,.F.);
#4583=ADVANCED_FACE('',(#687),#610,.F.);
#4584=ADVANCED_FACE('',(#688),#4518,.F.);
#4585=ADVANCED_FACE('',(#689,#561,#562),#611,.F.);
#4586=ADVANCED_FACE('',(#690),#4519,.F.);
#4587=ADVANCED_FACE('',(#691),#4520,.T.);
#4588=ADVANCED_FACE('',(#692,#563,#564),#612,.F.);
#4589=ADVANCED_FACE('',(#693),#4521,.T.);
#4590=ADVANCED_FACE('',(#694),#613,.F.);
#4591=ADVANCED_FACE('',(#695),#614,.F.);
#4592=ADVANCED_FACE('',(#696),#615,.T.);
#4593=ADVANCED_FACE('',(#697),#616,.T.);
#4594=ADVANCED_FACE('',(#698),#4522,.F.);
#4595=ADVANCED_FACE('',(#699,#565,#566),#617,.T.);
#4596=ADVANCED_FACE('',(#700),#4523,.F.);
#4597=ADVANCED_FACE('',(#701),#618,.T.);
#4598=ADVANCED_FACE('',(#702),#619,.T.);
#4599=ADVANCED_FACE('',(#703),#4524,.T.);
#4600=ADVANCED_FACE('',(#704,#567,#568),#620,.T.);
#4601=ADVANCED_FACE('',(#705),#4525,.T.);
#4602=ADVANCED_FACE('',(#706),#621,.T.);
#4603=ADVANCED_FACE('',(#707),#622,.T.);
#4722=CLOSED_SHELL('',(#4578,#4579,#4580,#4581,#4582,#4583,#4584,#4585,
#4586,#4587,#4588,#4589,#4590,#4591,#4592,#4593,#4594,#4595,#4596,#4597,
#4598,#4599,#4600,#4601,#4602,#4603));
#4832=AXIS2_PLACEMENT_3D('',#5830,#5100,#5101);
#4833=AXIS2_PLACEMENT_3D('',#5831,#5102,#5103);
#4834=AXIS2_PLACEMENT_3D('',#5833,#5104,#5105);
#4835=AXIS2_PLACEMENT_3D('',#5836,#5107,#5108);
#4836=AXIS2_PLACEMENT_3D('',#5837,#5109,#5110);
#4837=AXIS2_PLACEMENT_3D('',#5839,#5111,#5112);
#4838=AXIS2_PLACEMENT_3D('',#5842,#5114,#5115);
#4839=AXIS2_PLACEMENT_3D('',#5843,#5116,#5117);
#4840=AXIS2_PLACEMENT_3D('',#5845,#5118,#5119);
#4841=AXIS2_PLACEMENT_3D('',#5848,#5121,#5122);
#4842=AXIS2_PLACEMENT_3D('',#5849,#5123,#5124);
#4843=AXIS2_PLACEMENT_3D('',#5851,#5125,#5126);
#4844=AXIS2_PLACEMENT_3D('',#5854,#5128,#5129);
#4845=AXIS2_PLACEMENT_3D('',#5855,#5130,#5131);
#4846=AXIS2_PLACEMENT_3D('',#5864,#5136,#5137);
#4847=AXIS2_PLACEMENT_3D('',#5870,#5141,#5142);
#4848=AXIS2_PLACEMENT_3D('',#5872,#5143,#5144);
#4849=AXIS2_PLACEMENT_3D('',#5875,#5146,#5147);
#4850=AXIS2_PLACEMENT_3D('',#5876,#5148,#5149);
#4851=AXIS2_PLACEMENT_3D('',#5882,#5153,#5154);
#4852=AXIS2_PLACEMENT_3D('',#5884,#5155,#5156);
#4853=AXIS2_PLACEMENT_3D('',#5887,#5158,#5159);
#4854=AXIS2_PLACEMENT_3D('',#5888,#5160,#5161);
#4855=AXIS2_PLACEMENT_3D('',#5893,#5163,#5164);
#4856=AXIS2_PLACEMENT_3D('',#5896,#5166,#5167);
#4857=AXIS2_PLACEMENT_3D('',#5897,#5168,#5169);
#4858=AXIS2_PLACEMENT_3D('',#5903,#5173,#5174);
#4859=AXIS2_PLACEMENT_3D('',#5905,#5175,#5176);
#4860=AXIS2_PLACEMENT_3D('',#5908,#5178,#5179);
#4861=AXIS2_PLACEMENT_3D('',#5909,#5180,#5181);
#4862=AXIS2_PLACEMENT_3D('',#5912,#5184,#5185);
#4863=AXIS2_PLACEMENT_3D('',#5921,#5189,#5190);
#4864=AXIS2_PLACEMENT_3D('',#5925,#5192,#5193);
#4865=AXIS2_PLACEMENT_3D('',#5930,#5196,#5197);
#4866=AXIS2_PLACEMENT_3D('',#5933,#5199,#5200);
#4867=AXIS2_PLACEMENT_3D('',#5934,#5201,#5202);
#4868=AXIS2_PLACEMENT_3D('',#5940,#5206,#5207);
#4869=AXIS2_PLACEMENT_3D('',#5944,#5210,#5211);
#4870=AXIS2_PLACEMENT_3D('',#5946,#5212,#5213);
#4871=AXIS2_PLACEMENT_3D('',#5948,#5215,#5216);
#4872=AXIS2_PLACEMENT_3D('',#5952,#5219,#5220);
#4873=AXIS2_PLACEMENT_3D('',#5954,#5221,#5222);
#4874=AXIS2_PLACEMENT_3D('',#5956,#5224,#5225);
#4875=AXIS2_PLACEMENT_3D('',#5958,#5227,#5228);
#4876=AXIS2_PLACEMENT_3D('',#5962,#5231,#5232);
#4877=AXIS2_PLACEMENT_3D('',#5964,#5233,#5234);
#4878=AXIS2_PLACEMENT_3D('',#5966,#5236,#5237);
#4879=AXIS2_PLACEMENT_3D('',#5970,#5240,#5241);
#4880=AXIS2_PLACEMENT_3D('',#5972,#5242,#5243);
#4881=AXIS2_PLACEMENT_3D('',#5974,#5245,#5246);
#4882=AXIS2_PLACEMENT_3D('',#5976,#5248,#5249);
#5100=DIRECTION('axis',(0.,0.,1.));
#5101=DIRECTION('refdir',(1.,0.,0.));
#5102=DIRECTION('center_axis',(0.,1.,0.));
#5103=DIRECTION('ref_axis',(1.,0.,0.));
#5104=DIRECTION('center_axis',(0.,1.,0.));
#5105=DIRECTION('ref_axis',(1.,0.,0.));
#5106=DIRECTION('',(0.,1.,0.));
#5107=DIRECTION('center_axis',(0.,-1.,-8.88178419700126E-16));
#5108=DIRECTION('ref_axis',(1.,0.,0.));
#5109=DIRECTION('center_axis',(0.,1.,0.));
#5110=DIRECTION('ref_axis',(1.,0.,0.));
#5111=DIRECTION('center_axis',(0.,1.,-8.88178419700126E-16));
#5112=DIRECTION('ref_axis',(1.,0.,0.));
#5113=DIRECTION('',(0.,1.,0.));
#5114=DIRECTION('center_axis',(0.,-1.,0.));
#5115=DIRECTION('ref_axis',(1.,0.,0.));
#5116=DIRECTION('center_axis',(0.,1.,0.));
#5117=DIRECTION('ref_axis',(1.,0.,0.));
#5118=DIRECTION('center_axis',(0.,1.,0.));
#5119=DIRECTION('ref_axis',(1.,0.,0.));
#5120=DIRECTION('',(0.,1.,0.));
#5121=DIRECTION('center_axis',(0.,-1.,-8.88178419700126E-16));
#5122=DIRECTION('ref_axis',(1.,0.,0.));
#5123=DIRECTION('center_axis',(0.,1.,0.));
#5124=DIRECTION('ref_axis',(1.,0.,0.));
#5125=DIRECTION('center_axis',(0.,1.,-8.88178419700126E-16));
#5126=DIRECTION('ref_axis',(1.,0.,0.));
#5127=DIRECTION('',(0.,1.,0.));
#5128=DIRECTION('center_axis',(0.,-1.,0.));
#5129=DIRECTION('ref_axis',(1.,0.,0.));
#5130=DIRECTION('center_axis',(0.,1.,0.));
#5131=DIRECTION('ref_axis',(0.,0.,1.));
#5132=DIRECTION('',(-1.,0.,0.));
#5133=DIRECTION('',(0.,0.,-1.));
#5134=DIRECTION('',(1.,0.,0.));
#5135=DIRECTION('',(0.,0.,1.));
#5136=DIRECTION('center_axis',(0.,0.,1.));
#5137=DIRECTION('ref_axis',(0.,-1.,0.));
#5138=DIRECTION('',(0.,1.,0.));
#5139=DIRECTION('',(1.,0.,0.));
#5140=DIRECTION('',(0.,-1.,0.));
#5141=DIRECTION('center_axis',(-1.,0.,0.));
#5142=DIRECTION('ref_axis',(0.,5.92118946466746E-15,1.));
#5143=DIRECTION('center_axis',(-1.,0.,0.));
#5144=DIRECTION('ref_axis',(0.,5.92118946466746E-15,1.));
#5145=DIRECTION('',(1.,0.,0.));
#5146=DIRECTION('center_axis',(1.,0.,0.));
#5147=DIRECTION('ref_axis',(0.,5.92118946466746E-15,1.));
#5148=DIRECTION('center_axis',(0.,1.,-8.88178419700126E-16));
#5149=DIRECTION('ref_axis',(0.,8.88178419700126E-16,1.));
#5150=DIRECTION('',(0.,-8.88178419700126E-16,-1.));
#5151=DIRECTION('',(1.,0.,0.));
#5152=DIRECTION('',(0.,8.88178419700126E-16,1.));
#5153=DIRECTION('center_axis',(-1.,0.,0.));
#5154=DIRECTION('ref_axis',(0.,1.,-8.88178419700118E-15));
#5155=DIRECTION('center_axis',(-1.,0.,0.));
#5156=DIRECTION('ref_axis',(0.,1.,-8.88178419700118E-15));
#5157=DIRECTION('',(1.,0.,0.));
#5158=DIRECTION('center_axis',(1.,0.,0.));
#5159=DIRECTION('ref_axis',(0.,1.,-8.88178419700118E-15));
#5160=DIRECTION('center_axis',(-1.,0.,0.));
#5161=DIRECTION('ref_axis',(0.,1.,-7.58652400160517E-15));
#5162=DIRECTION('',(1.,0.,0.));
#5163=DIRECTION('center_axis',(1.,0.,0.));
#5164=DIRECTION('ref_axis',(0.,1.,-7.58652400160517E-15));
#5165=DIRECTION('',(1.,0.,0.));
#5166=DIRECTION('center_axis',(-1.,0.,0.));
#5167=DIRECTION('ref_axis',(0.,1.,-7.58652400160517E-15));
#5168=DIRECTION('center_axis',(0.,-1.,0.));
#5169=DIRECTION('ref_axis',(0.,0.,-1.));
#5170=DIRECTION('',(0.,0.,1.));
#5171=DIRECTION('',(1.,0.,0.));
#5172=DIRECTION('',(0.,0.,-1.));
#5173=DIRECTION('center_axis',(-1.,0.,0.));
#5174=DIRECTION('ref_axis',(0.,5.92118946466745E-15,1.));
#5175=DIRECTION('center_axis',(1.,0.,0.));
#5176=DIRECTION('ref_axis',(0.,5.92118946466745E-15,1.));
#5177=DIRECTION('',(1.,0.,0.));
#5178=DIRECTION('center_axis',(-1.,0.,0.));
#5179=DIRECTION('ref_axis',(0.,5.92118946466745E-15,1.));
#5180=DIRECTION('center_axis',(0.,0.,-1.));
#5181=DIRECTION('ref_axis',(0.,1.,0.));
#5182=DIRECTION('',(0.,-1.,0.));
#5183=DIRECTION('',(0.,1.,0.));
#5184=DIRECTION('center_axis',(1.,0.,0.));
#5185=DIRECTION('ref_axis',(0.,1.,0.));
#5186=DIRECTION('',(0.,1.,0.));
#5187=DIRECTION('',(0.,0.,-1.));
#5188=DIRECTION('',(0.,-1.,0.));
#5189=DIRECTION('center_axis',(1.,0.,0.));
#5190=DIRECTION('ref_axis',(0.,-5.92118946466746E-15,1.));
#5191=DIRECTION('',(0.,8.88178419700126E-16,-1.));
#5192=DIRECTION('center_axis',(1.,0.,0.));
#5193=DIRECTION('ref_axis',(0.,-1.,-8.88178419700118E-15));
#5194=DIRECTION('',(0.,1.,-7.61818177922111E-18));
#5195=DIRECTION('',(0.,1.,-1.49625744558646E-17));
#5196=DIRECTION('center_axis',(-1.,0.,0.));
#5197=DIRECTION('ref_axis',(0.,-1.,-7.58652400160517E-15));
#5198=DIRECTION('',(0.,0.,1.));
#5199=DIRECTION('center_axis',(-1.,0.,0.));
#5200=DIRECTION('ref_axis',(0.,-5.92118946466745E-15,1.));
#5201=DIRECTION('center_axis',(0.,1.,0.));
#5202=DIRECTION('ref_axis',(0.,0.,1.));
#5203=DIRECTION('',(-1.,0.,0.));
#5204=DIRECTION('',(0.,0.,1.));
#5205=DIRECTION('',(1.,0.,0.));
#5206=DIRECTION('center_axis',(0.,0.,-1.));
#5207=DIRECTION('ref_axis',(0.,1.,0.));
#5208=DIRECTION('',(0.,1.,0.));
#5209=DIRECTION('',(1.,0.,0.));
#5210=DIRECTION('center_axis',(1.,0.,0.));
#5211=DIRECTION('ref_axis',(0.,-5.92118946466746E-15,1.));
#5212=DIRECTION('center_axis',(-1.,0.,0.));
#5213=DIRECTION('ref_axis',(0.,-5.92118946466746E-15,1.));
#5214=DIRECTION('',(1.,0.,0.));
#5215=DIRECTION('center_axis',(0.,1.,8.88178419700126E-16));
#5216=DIRECTION('ref_axis',(0.,-8.88178419700126E-16,1.));
#5217=DIRECTION('',(0.,-8.88178419700126E-16,1.));
#5218=DIRECTION('',(1.,0.,0.));
#5219=DIRECTION('center_axis',(1.,0.,0.));
#5220=DIRECTION('ref_axis',(0.,-1.,-8.88178419700118E-15));
#5221=DIRECTION('center_axis',(-1.,0.,0.));
#5222=DIRECTION('ref_axis',(0.,-1.,-8.88178419700118E-15));
#5223=DIRECTION('',(1.,0.,0.));
#5224=DIRECTION('center_axis',(0.,7.61818177922111E-18,1.));
#5225=DIRECTION('ref_axis',(0.,-1.,7.61818177922111E-18));
#5226=DIRECTION('',(0.,1.,7.61818177922111E-18));
#5227=DIRECTION('center_axis',(0.,1.49625744558646E-17,-1.));
#5228=DIRECTION('ref_axis',(0.,1.,1.49625744558646E-17));
#5229=DIRECTION('',(0.,1.,1.49625744558646E-17));
#5230=DIRECTION('',(1.,0.,0.));
#5231=DIRECTION('center_axis',(1.,0.,0.));
#5232=DIRECTION('ref_axis',(0.,-1.,-7.58652400160517E-15));
#5233=DIRECTION('center_axis',(1.,0.,0.));
#5234=DIRECTION('ref_axis',(0.,-1.,-7.58652400160517E-15));
#5235=DIRECTION('',(1.,0.,0.));
#5236=DIRECTION('center_axis',(0.,-1.,0.));
#5237=DIRECTION('ref_axis',(0.,0.,-1.));
#5238=DIRECTION('',(0.,0.,-1.));
#5239=DIRECTION('',(1.,0.,0.));
#5240=DIRECTION('center_axis',(1.,0.,0.));
#5241=DIRECTION('ref_axis',(0.,-5.92118946466745E-15,1.));
#5242=DIRECTION('center_axis',(1.,0.,0.));
#5243=DIRECTION('ref_axis',(0.,-5.92118946466745E-15,1.));
#5244=DIRECTION('',(1.,0.,0.));
#5245=DIRECTION('center_axis',(0.,0.,1.));
#5246=DIRECTION('ref_axis',(0.,-1.,0.));
#5247=DIRECTION('',(0.,-1.,0.));
#5248=DIRECTION('center_axis',(1.,0.,0.));
#5249=DIRECTION('ref_axis',(0.,1.,0.));
#5830=CARTESIAN_POINT('',(0.,0.,0.));
#5831=CARTESIAN_POINT('Origin',(-54.7683231875009,0.,15.));
#5832=CARTESIAN_POINT('',(-62.2683231875009,-114.3,15.));
#5833=CARTESIAN_POINT('Origin',(-54.7683231875009,-114.3,15.));
#5834=CARTESIAN_POINT('',(-62.2683231875009,-112.3,15.));
#5835=CARTESIAN_POINT('',(-62.2683231875009,0.,15.));
#5836=CARTESIAN_POINT('Origin',(-54.7683231875009,-112.3,15.));
#5837=CARTESIAN_POINT('Origin',(-54.7683231875009,0.,15.));
#5838=CARTESIAN_POINT('',(-62.2683231875009,112.3,15.));
#5839=CARTESIAN_POINT('Origin',(-54.7683231875009,112.3,15.));
#5840=CARTESIAN_POINT('',(-62.2683231875009,114.3,15.));
#5841=CARTESIAN_POINT('',(-62.2683231875009,0.,15.));
#5842=CARTESIAN_POINT('Origin',(-54.7683231875009,114.3,15.));
#5843=CARTESIAN_POINT('Origin',(175.231676812499,0.,15.));
#5844=CARTESIAN_POINT('',(167.731676812499,-114.3,15.));
#5845=CARTESIAN_POINT('Origin',(175.231676812499,-114.3,15.));
#5846=CARTESIAN_POINT('',(167.731676812499,-112.3,15.));
#5847=CARTESIAN_POINT('',(167.731676812499,0.,15.));
#5848=CARTESIAN_POINT('Origin',(175.231676812499,-112.3,15.));
#5849=CARTESIAN_POINT('Origin',(175.231676812499,0.,15.));
#5850=CARTESIAN_POINT('',(167.731676812499,112.3,15.));
#5851=CARTESIAN_POINT('Origin',(175.231676812499,112.3,15.));
#5852=CARTESIAN_POINT('',(167.731676812499,114.3,15.));
#5853=CARTESIAN_POINT('',(167.731676812499,0.,15.));
#5854=CARTESIAN_POINT('Origin',(175.231676812499,114.3,15.));
#5855=CARTESIAN_POINT('Origin',(0.,99.3,28.));
#5856=CARTESIAN_POINT('',(198.,99.3,30.));
#5857=CARTESIAN_POINT('',(-198.,99.3,30.));
#5858=CARTESIAN_POINT('',(0.,99.3,30.));
#5859=CARTESIAN_POINT('',(-198.,99.3,28.));
#5860=CARTESIAN_POINT('',(-198.,99.3,30.));
#5861=CARTESIAN_POINT('',(198.,99.3,28.));
#5862=CARTESIAN_POINT('',(0.,99.3,28.));
#5863=CARTESIAN_POINT('',(198.,99.3,30.));
#5864=CARTESIAN_POINT('Origin',(0.,109.3,28.));
#5865=CARTESIAN_POINT('',(-198.,109.3,28.));
#5866=CARTESIAN_POINT('',(-198.,112.3,28.));
#5867=CARTESIAN_POINT('',(198.,109.3,28.));
#5868=CARTESIAN_POINT('',(0.,109.3,28.));
#5869=CARTESIAN_POINT('',(198.,112.3,28.));
#5870=CARTESIAN_POINT('Origin',(0.,109.3,25.));
#5871=CARTESIAN_POINT('',(-198.,112.3,25.));
#5872=CARTESIAN_POINT('Origin',(-198.,109.3,25.));
#5873=CARTESIAN_POINT('',(198.,112.3,25.));
#5874=CARTESIAN_POINT('',(0.,112.3,25.));
#5875=CARTESIAN_POINT('Origin',(198.,109.3,25.));
#5876=CARTESIAN_POINT('Origin',(0.,112.3,5.));
#5877=CARTESIAN_POINT('',(-198.,112.3,5.));
#5878=CARTESIAN_POINT('',(-198.,112.3,5.));
#5879=CARTESIAN_POINT('',(198.,112.3,5.));
#5880=CARTESIAN_POINT('',(0.,112.3,5.));
#5881=CARTESIAN_POINT('',(198.,112.3,5.));
#5882=CARTESIAN_POINT('Origin',(0.,109.3,5.00000000000003));
#5883=CARTESIAN_POINT('',(-198.,109.3,2.));
#5884=CARTESIAN_POINT('Origin',(-198.,109.3,5.00000000000003));
#5885=CARTESIAN_POINT('',(198.,109.3,2.));
#5886=CARTESIAN_POINT('',(0.,109.3,2.));
#5887=CARTESIAN_POINT('Origin',(198.,109.3,5.00000000000003));
#5888=CARTESIAN_POINT('Origin',(0.,111.3,3.00000000000002));
#5889=CARTESIAN_POINT('',(-198.,111.3,0.));
#5890=CARTESIAN_POINT('',(198.,111.3,0.));
#5891=CARTESIAN_POINT('',(0.,111.3,-2.22044604925031E-15));
#5892=CARTESIAN_POINT('',(-198.,114.3,3.));
#5893=CARTESIAN_POINT('Origin',(-198.,111.3,3.00000000000002));
#5894=CARTESIAN_POINT('',(198.,114.3,3.));
#5895=CARTESIAN_POINT('',(0.,114.3,3.));
#5896=CARTESIAN_POINT('Origin',(198.,111.3,3.00000000000002));
#5897=CARTESIAN_POINT('Origin',(0.,114.3,27.));
#5898=CARTESIAN_POINT('',(-198.,114.3,27.));
#5899=CARTESIAN_POINT('',(-198.,114.3,3.));
#5900=CARTESIAN_POINT('',(198.,114.3,27.));
#5901=CARTESIAN_POINT('',(0.,114.3,27.));
#5902=CARTESIAN_POINT('',(198.,114.3,3.));
#5903=CARTESIAN_POINT('Origin',(0.,111.3,27.));
#5904=CARTESIAN_POINT('',(-198.,111.3,30.));
#5905=CARTESIAN_POINT('Origin',(-198.,111.3,27.));
#5906=CARTESIAN_POINT('',(198.,111.3,30.));
#5907=CARTESIAN_POINT('',(0.,111.3,30.));
#5908=CARTESIAN_POINT('Origin',(198.,111.3,27.));
#5909=CARTESIAN_POINT('Origin',(0.,99.3,30.));
#5910=CARTESIAN_POINT('',(-198.,111.3,30.));
#5911=CARTESIAN_POINT('',(198.,111.3,30.));
#5912=CARTESIAN_POINT('Origin',(-198.,-57.15,15.));
#5913=CARTESIAN_POINT('',(-198.,-111.3,30.));
#5914=CARTESIAN_POINT('',(-198.,-99.3,30.));
#5915=CARTESIAN_POINT('',(-198.,-111.3,30.));
#5916=CARTESIAN_POINT('',(-198.,-99.3,28.));
#5917=CARTESIAN_POINT('',(-198.,-99.3,30.));
#5918=CARTESIAN_POINT('',(-198.,-109.3,28.));
#5919=CARTESIAN_POINT('',(-198.,-112.3,28.));
#5920=CARTESIAN_POINT('',(-198.,-112.3,25.));
#5921=CARTESIAN_POINT('Origin',(-198.,-109.3,25.));
#5922=CARTESIAN_POINT('',(-198.,-112.3,5.));
#5923=CARTESIAN_POINT('',(-198.,-112.3,5.));
#5924=CARTESIAN_POINT('',(-198.,-109.3,2.));
#5925=CARTESIAN_POINT('Origin',(-198.,-109.3,5.00000000000003));
#5926=CARTESIAN_POINT('',(-198.,0.,2.));
#5927=CARTESIAN_POINT('',(-198.,-111.3,0.));
#5928=CARTESIAN_POINT('',(-198.,0.,0.));
#5929=CARTESIAN_POINT('',(-198.,-114.3,3.));
#5930=CARTESIAN_POINT('Origin',(-198.,-111.3,3.00000000000002));
#5931=CARTESIAN_POINT('',(-198.,-114.3,27.));
#5932=CARTESIAN_POINT('',(-198.,-114.3,3.));
#5933=CARTESIAN_POINT('Origin',(-198.,-111.3,27.));
#5934=CARTESIAN_POINT('Origin',(0.,-99.3,28.));
#5935=CARTESIAN_POINT('',(198.,-99.3,30.));
#5936=CARTESIAN_POINT('',(0.,-99.3,30.));
#5937=CARTESIAN_POINT('',(198.,-99.3,28.));
#5938=CARTESIAN_POINT('',(198.,-99.3,30.));
#5939=CARTESIAN_POINT('',(0.,-99.3,28.));
#5940=CARTESIAN_POINT('Origin',(0.,-109.3,28.));
#5941=CARTESIAN_POINT('',(198.,-109.3,28.));
#5942=CARTESIAN_POINT('',(198.,-112.3,28.));
#5943=CARTESIAN_POINT('',(0.,-109.3,28.));
#5944=CARTESIAN_POINT('Origin',(0.,-109.3,25.));
#5945=CARTESIAN_POINT('',(198.,-112.3,25.));
#5946=CARTESIAN_POINT('Origin',(198.,-109.3,25.));
#5947=CARTESIAN_POINT('',(0.,-112.3,25.));
#5948=CARTESIAN_POINT('Origin',(0.,-112.3,5.));
#5949=CARTESIAN_POINT('',(198.,-112.3,5.));
#5950=CARTESIAN_POINT('',(198.,-112.3,5.));
#5951=CARTESIAN_POINT('',(0.,-112.3,5.));
#5952=CARTESIAN_POINT('Origin',(0.,-109.3,5.00000000000003));
#5953=CARTESIAN_POINT('',(198.,-109.3,2.));
#5954=CARTESIAN_POINT('Origin',(198.,-109.3,5.00000000000003));
#5955=CARTESIAN_POINT('',(0.,-109.3,2.));
#5956=CARTESIAN_POINT('Origin',(0.,0.,2.));
#5957=CARTESIAN_POINT('',(198.,0.,2.));
#5958=CARTESIAN_POINT('Origin',(0.,-111.3,-1.66533453693773E-15));
#5959=CARTESIAN_POINT('',(198.,-111.3,0.));
#5960=CARTESIAN_POINT('',(198.,0.,0.));
#5961=CARTESIAN_POINT('',(0.,-111.3,-2.22044604925031E-15));
#5962=CARTESIAN_POINT('Origin',(0.,-111.3,3.00000000000002));
#5963=CARTESIAN_POINT('',(198.,-114.3,3.));
#5964=CARTESIAN_POINT('Origin',(198.,-111.3,3.00000000000002));
#5965=CARTESIAN_POINT('',(0.,-114.3,3.));
#5966=CARTESIAN_POINT('Origin',(0.,-114.3,27.));
#5967=CARTESIAN_POINT('',(198.,-114.3,27.));
#5968=CARTESIAN_POINT('',(198.,-114.3,3.));
#5969=CARTESIAN_POINT('',(0.,-114.3,27.));
#5970=CARTESIAN_POINT('Origin',(0.,-111.3,27.));
#5971=CARTESIAN_POINT('',(198.,-111.3,30.));
#5972=CARTESIAN_POINT('Origin',(198.,-111.3,27.));
#5973=CARTESIAN_POINT('',(0.,-111.3,30.));
#5974=CARTESIAN_POINT('Origin',(0.,-99.3,30.));
#5975=CARTESIAN_POINT('',(198.,-111.3,30.));
#5976=CARTESIAN_POINT('Origin',(198.,-57.15,15.));
#74503=UNCERTAINTY_MEASURE_WITH_UNIT(LENGTH_MEASURE(0.01),#74524,
'DISTANCE_ACCURACY_VALUE',
'Maximum model space distance between geometric entities at asserted c
onnectivities');
#74512=UNCERTAINTY_MEASURE_WITH_UNIT(LENGTH_MEASURE(0.01),#74524,
'DISTANCE_ACCURACY_VALUE',
'Maximum model space distance between geometric entities at asserted c
onnectivities');
#74514=(
GEOMETRIC_REPRESENTATION_CONTEXT(3)
GLOBAL_UNCERTAINTY_ASSIGNED_CONTEXT((#74503))
GLOBAL_UNIT_ASSIGNED_CONTEXT((#74524,#74526,#74527))
REPRESENTATION_CONTEXT('','3D')
);
#74523=(
GEOMETRIC_REPRESENTATION_CONTEXT(3)
GLOBAL_UNCERTAINTY_ASSIGNED_CONTEXT((#74512))
GLOBAL_UNIT_ASSIGNED_CONTEXT((#74524,#74526,#74527))
REPRESENTATION_CONTEXT('','3D')
);
#74524=(
LENGTH_UNIT()
NAMED_UNIT(*)
SI_UNIT(.MILLI.,.METRE.)
);
#74526=(
NAMED_UNIT(*)
PLANE_ANGLE_UNIT()
SI_UNIT($,.RADIAN.)
);
#74527=(
NAMED_UNIT(*)
SI_UNIT($,.STERADIAN.)
SOLID_ANGLE_UNIT()
);
#74529=SHAPE_DEFINITION_REPRESENTATION(#74539,#74558);
#74539=PRODUCT_DEFINITION_SHAPE('',$,#74569);
#74558=SHAPE_REPRESENTATION('',(#4832),#74514);
#74567=PRODUCT_DEFINITION_CONTEXT('part definition',#74599,'design');
#74569=PRODUCT_DEFINITION('Bottom_Base','Bottom_Base',#74579,#74567);
#74579=PRODUCT_DEFINITION_FORMATION('',$,#74602);
#74599=APPLICATION_CONTEXT(
'Core Data for Automotive Mechanical Design Process');
#74600=PRODUCT_CONTEXT('part definition',#74599,'mechanical');
#74602=PRODUCT('Bottom_Base','Bottom_Base',$,(#74600));
#74612=PRESENTATION_STYLE_ASSIGNMENT((#74615));
#74615=SURFACE_STYLE_USAGE(.BOTH.,#74618);
#74618=SURFACE_SIDE_STYLE('',(#74621));
#74621=SURFACE_STYLE_FILL_AREA(#74624);
#74624=FILL_AREA_STYLE('Opaque(215,0,0)',(#74627));
#74627=FILL_AREA_STYLE_COLOUR('Opaque(215,0,0)',#74630);
#74630=COLOUR_RGB('Opaque(215,0,0)', 0.09019608, 0.27058824, 0.51372549);
ENDSEC;
END-ISO-10303-21;
